ISO-10303-21;
HEADER;
/* Generated by software containing ST-Developer
 * from STEP Tools, Inc. (www.steptools.com) 
 */

FILE_DESCRIPTION(
/* description */ (''),
/* implementation_level */ '2;1');

FILE_NAME(
/* name */ 'Circuit.step',
/* time_stamp */ '2026-10-23T22:29:29+06:00',
/* author */ (''),
/* organization */ (''),
/* preprocessor_version */ 'ST-DEVELOPER v20.2',
/* originating_system */ 'Autodesk Translation Framework v15.15.0.0',
/* authorisation */ '');

FILE_SCHEMA (('AUTOMOTIVE_DESIGN { 1 0 10303 214 3 1 1 }'));
ENDSEC;

DATA;
#10=MECHANICAL_DESIGN_GEOMETRIC_PRESENTATION_REPRESENTATION('',(#81,#82,#83,#84),#7047);
#61=SHAPE_REPRESENTATION_RELATIONSHIP('SRR','None',#7094,#71);
#71=ADVANCED_BREP_SHAPE_REPRESENTATION('',(#94),#7046);
#81=STYLED_ITEM('',(#7212),#3385);
#82=STYLED_ITEM('',(#7212),#3392);
#83=STYLED_ITEM('',(#7212),#3395);
#84=STYLED_ITEM('',(#7212),#94);
#94=MANIFOLD_SOLID_BREP('Circuit',#3406);
#123=FACE_BOUND('',#649,.T.);
#124=FACE_BOUND('',#660,.T.);
#250=PLANE('',#3866);
#251=PLANE('',#3867);
#252=PLANE('',#3868);
#253=PLANE('',#3869);
#254=PLANE('',#3870);
#255=PLANE('',#3871);
#256=PLANE('',#3872);
#257=PLANE('',#3873);
#258=PLANE('',#3874);
#259=PLANE('',#3875);
#260=PLANE('',#3876);
#261=PLANE('',#3877);
#262=PLANE('',#3878);
#263=PLANE('',#3879);
#264=PLANE('',#3880);
#265=PLANE('',#3881);
#439=FACE_OUTER_BOUND('',#644,.T.);
#440=FACE_OUTER_BOUND('',#645,.T.);
#441=FACE_OUTER_BOUND('',#646,.T.);
#442=FACE_OUTER_BOUND('',#647,.T.);
#443=FACE_OUTER_BOUND('',#648,.T.);
#444=FACE_OUTER_BOUND('',#650,.T.);
#445=FACE_OUTER_BOUND('',#651,.T.);
#446=FACE_OUTER_BOUND('',#652,.T.);
#447=FACE_OUTER_BOUND('',#653,.T.);
#448=FACE_OUTER_BOUND('',#654,.T.);
#449=FACE_OUTER_BOUND('',#655,.T.);
#450=FACE_OUTER_BOUND('',#656,.T.);
#451=FACE_OUTER_BOUND('',#657,.T.);
#452=FACE_OUTER_BOUND('',#658,.T.);
#453=FACE_OUTER_BOUND('',#659,.T.);
#454=FACE_OUTER_BOUND('',#661,.T.);
#644=EDGE_LOOP('',(#3101,#3102,#3103,#3104));
#645=EDGE_LOOP('',(#3105,#3106,#3107,#3108));
#646=EDGE_LOOP('',(#3109,#3110,#3111,#3112));
#647=EDGE_LOOP('',(#3113,#3114,#3115,#3116));
#648=EDGE_LOOP('',(#3117,#3118,#3119,#3120));
#649=EDGE_LOOP('',(#3121,#3122,#3123,#3124));
#650=EDGE_LOOP('',(#3125,#3126,#3127,#3128));
#651=EDGE_LOOP('',(#3129,#3130,#3131,#3132));
#652=EDGE_LOOP('',(#3133,#3134,#3135,#3136));
#653=EDGE_LOOP('',(#3137,#3138,#3139,#3140));
#654=EDGE_LOOP('',(#3141,#3142,#3143,#3144));
#655=EDGE_LOOP('',(#3145,#3146,#3147,#3148));
#656=EDGE_LOOP('',(#3149,#3150,#3151,#3152));
#657=EDGE_LOOP('',(#3153,#3154,#3155,#3156));
#658=EDGE_LOOP('',(#3157,#3158,#3159,#3160));
#659=EDGE_LOOP('',(#3161,#3162,#3163,#3164));
#660=EDGE_LOOP('',(#3165,#3166,#3167,#3168));
#661=EDGE_LOOP('',(#3169,#3170,#3171,#3172));
#1085=LINE('',#6941,#1379);
#1086=LINE('',#6943,#1380);
#1087=LINE('',#6945,#1381);
#1088=LINE('',#6946,#1382);
#1089=LINE('',#6949,#1383);
#1090=LINE('',#6951,#1384);
#1091=LINE('',#6952,#1385);
#1092=LINE('',#6955,#1386);
#1093=LINE('',#6957,#1387);
#1094=LINE('',#6958,#1388);
#1095=LINE('',#6960,#1389);
#1096=LINE('',#6961,#1390);
#1097=LINE('',#6965,#1391);
#1098=LINE('',#6967,#1392);
#1099=LINE('',#6969,#1393);
#1100=LINE('',#6970,#1394);
#1101=LINE('',#6973,#1395);
#1102=LINE('',#6975,#1396);
#1103=LINE('',#6976,#1397);
#1104=LINE('',#6979,#1398);
#1105=LINE('',#6980,#1399);
#1106=LINE('',#6984,#1400);
#1107=LINE('',#6986,#1401);
#1108=LINE('',#6988,#1402);
#1109=LINE('',#6989,#1403);
#1110=LINE('',#6992,#1404);
#1111=LINE('',#6994,#1405);
#1112=LINE('',#6995,#1406);
#1113=LINE('',#6998,#1407);
#1114=LINE('',#7000,#1408);
#1115=LINE('',#7001,#1409);
#1116=LINE('',#7003,#1410);
#1117=LINE('',#7004,#1411);
#1118=LINE('',#7008,#1412);
#1119=LINE('',#7009,#1413);
#1120=LINE('',#7011,#1414);
#1379=VECTOR('',#4848,10.);
#1380=VECTOR('',#4849,10.);
#1381=VECTOR('',#4850,10.);
#1382=VECTOR('',#4851,10.);
#1383=VECTOR('',#4854,10.);
#1384=VECTOR('',#4855,10.);
#1385=VECTOR('',#4856,10.);
#1386=VECTOR('',#4859,10.);
#1387=VECTOR('',#4860,10.);
#1388=VECTOR('',#4861,10.);
#1389=VECTOR('',#4864,10.);
#1390=VECTOR('',#4865,10.);
#1391=VECTOR('',#4868,10.);
#1392=VECTOR('',#4869,10.);
#1393=VECTOR('',#4870,10.);
#1394=VECTOR('',#4871,10.);
#1395=VECTOR('',#4874,10.);
#1396=VECTOR('',#4875,10.);
#1397=VECTOR('',#4876,10.);
#1398=VECTOR('',#4879,10.);
#1399=VECTOR('',#4880,10.);
#1400=VECTOR('',#4883,10.);
#1401=VECTOR('',#4884,10.);
#1402=VECTOR('',#4885,10.);
#1403=VECTOR('',#4886,10.);
#1404=VECTOR('',#4889,10.);
#1405=VECTOR('',#4890,10.);
#1406=VECTOR('',#4891,10.);
#1407=VECTOR('',#4894,10.);
#1408=VECTOR('',#4895,10.);
#1409=VECTOR('',#4896,10.);
#1410=VECTOR('',#4899,10.);
#1411=VECTOR('',#4900,10.);
#1412=VECTOR('',#4905,10.);
#1413=VECTOR('',#4906,10.);
#1414=VECTOR('',#4909,10.);
#1721=VERTEX_POINT('',#6939);
#1722=VERTEX_POINT('',#6940);
#1723=VERTEX_POINT('',#6942);
#1724=VERTEX_POINT('',#6944);
#1725=VERTEX_POINT('',#6948);
#1726=VERTEX_POINT('',#6950);
#1727=VERTEX_POINT('',#6954);
#1728=VERTEX_POINT('',#6956);
#1729=VERTEX_POINT('',#6963);
#1730=VERTEX_POINT('',#6964);
#1731=VERTEX_POINT('',#6966);
#1732=VERTEX_POINT('',#6968);
#1733=VERTEX_POINT('',#6972);
#1734=VERTEX_POINT('',#6974);
#1735=VERTEX_POINT('',#6978);
#1736=VERTEX_POINT('',#6982);
#1737=VERTEX_POINT('',#6983);
#1738=VERTEX_POINT('',#6985);
#1739=VERTEX_POINT('',#6987);
#1740=VERTEX_POINT('',#6991);
#1741=VERTEX_POINT('',#6993);
#1742=VERTEX_POINT('',#6997);
#1743=VERTEX_POINT('',#6999);
#1744=VERTEX_POINT('',#7007);
#2185=EDGE_CURVE('',#1721,#1722,#1085,.T.);
#2186=EDGE_CURVE('',#1721,#1723,#1086,.T.);
#2187=EDGE_CURVE('',#1723,#1724,#1087,.T.);
#2188=EDGE_CURVE('',#1722,#1724,#1088,.T.);
#2189=EDGE_CURVE('',#1725,#1721,#1089,.T.);
#2190=EDGE_CURVE('',#1725,#1726,#1090,.T.);
#2191=EDGE_CURVE('',#1726,#1723,#1091,.T.);
#2192=EDGE_CURVE('',#1727,#1725,#1092,.T.);
#2193=EDGE_CURVE('',#1727,#1728,#1093,.T.);
#2194=EDGE_CURVE('',#1728,#1726,#1094,.T.);
#2195=EDGE_CURVE('',#1722,#1727,#1095,.T.);
#2196=EDGE_CURVE('',#1724,#1728,#1096,.T.);
#2197=EDGE_CURVE('',#1729,#1730,#1097,.T.);
#2198=EDGE_CURVE('',#1731,#1729,#1098,.T.);
#2199=EDGE_CURVE('',#1732,#1731,#1099,.T.);
#2200=EDGE_CURVE('',#1730,#1732,#1100,.T.);
#2201=EDGE_CURVE('',#1729,#1733,#1101,.T.);
#2202=EDGE_CURVE('',#1734,#1733,#1102,.T.);
#2203=EDGE_CURVE('',#1731,#1734,#1103,.T.);
#2204=EDGE_CURVE('',#1730,#1735,#1104,.T.);
#2205=EDGE_CURVE('',#1733,#1735,#1105,.T.);
#2206=EDGE_CURVE('',#1736,#1737,#1106,.T.);
#2207=EDGE_CURVE('',#1736,#1738,#1107,.T.);
#2208=EDGE_CURVE('',#1738,#1739,#1108,.T.);
#2209=EDGE_CURVE('',#1737,#1739,#1109,.T.);
#2210=EDGE_CURVE('',#1740,#1736,#1110,.T.);
#2211=EDGE_CURVE('',#1740,#1741,#1111,.T.);
#2212=EDGE_CURVE('',#1741,#1738,#1112,.T.);
#2213=EDGE_CURVE('',#1742,#1740,#1113,.T.);
#2214=EDGE_CURVE('',#1742,#1743,#1114,.T.);
#2215=EDGE_CURVE('',#1743,#1741,#1115,.T.);
#2216=EDGE_CURVE('',#1737,#1742,#1116,.T.);
#2217=EDGE_CURVE('',#1739,#1743,#1117,.T.);
#2218=EDGE_CURVE('',#1744,#1734,#1118,.T.);
#2219=EDGE_CURVE('',#1732,#1744,#1119,.T.);
#2220=EDGE_CURVE('',#1735,#1744,#1120,.T.);
#3101=ORIENTED_EDGE('',*,*,#2185,.F.);
#3102=ORIENTED_EDGE('',*,*,#2186,.T.);
#3103=ORIENTED_EDGE('',*,*,#2187,.T.);
#3104=ORIENTED_EDGE('',*,*,#2188,.F.);
#3105=ORIENTED_EDGE('',*,*,#2189,.F.);
#3106=ORIENTED_EDGE('',*,*,#2190,.T.);
#3107=ORIENTED_EDGE('',*,*,#2191,.T.);
#3108=ORIENTED_EDGE('',*,*,#2186,.F.);
#3109=ORIENTED_EDGE('',*,*,#2192,.F.);
#3110=ORIENTED_EDGE('',*,*,#2193,.T.);
#3111=ORIENTED_EDGE('',*,*,#2194,.T.);
#3112=ORIENTED_EDGE('',*,*,#2190,.F.);
#3113=ORIENTED_EDGE('',*,*,#2195,.F.);
#3114=ORIENTED_EDGE('',*,*,#2188,.T.);
#3115=ORIENTED_EDGE('',*,*,#2196,.T.);
#3116=ORIENTED_EDGE('',*,*,#2193,.F.);
#3117=ORIENTED_EDGE('',*,*,#2197,.F.);
#3118=ORIENTED_EDGE('',*,*,#2198,.F.);
#3119=ORIENTED_EDGE('',*,*,#2199,.F.);
#3120=ORIENTED_EDGE('',*,*,#2200,.F.);
#3121=ORIENTED_EDGE('',*,*,#2196,.F.);
#3122=ORIENTED_EDGE('',*,*,#2187,.F.);
#3123=ORIENTED_EDGE('',*,*,#2191,.F.);
#3124=ORIENTED_EDGE('',*,*,#2194,.F.);
#3125=ORIENTED_EDGE('',*,*,#2198,.T.);
#3126=ORIENTED_EDGE('',*,*,#2201,.T.);
#3127=ORIENTED_EDGE('',*,*,#2202,.F.);
#3128=ORIENTED_EDGE('',*,*,#2203,.F.);
#3129=ORIENTED_EDGE('',*,*,#2197,.T.);
#3130=ORIENTED_EDGE('',*,*,#2204,.T.);
#3131=ORIENTED_EDGE('',*,*,#2205,.F.);
#3132=ORIENTED_EDGE('',*,*,#2201,.F.);
#3133=ORIENTED_EDGE('',*,*,#2206,.F.);
#3134=ORIENTED_EDGE('',*,*,#2207,.T.);
#3135=ORIENTED_EDGE('',*,*,#2208,.T.);
#3136=ORIENTED_EDGE('',*,*,#2209,.F.);
#3137=ORIENTED_EDGE('',*,*,#2210,.F.);
#3138=ORIENTED_EDGE('',*,*,#2211,.T.);
#3139=ORIENTED_EDGE('',*,*,#2212,.T.);
#3140=ORIENTED_EDGE('',*,*,#2207,.F.);
#3141=ORIENTED_EDGE('',*,*,#2213,.F.);
#3142=ORIENTED_EDGE('',*,*,#2214,.T.);
#3143=ORIENTED_EDGE('',*,*,#2215,.T.);
#3144=ORIENTED_EDGE('',*,*,#2211,.F.);
#3145=ORIENTED_EDGE('',*,*,#2216,.F.);
#3146=ORIENTED_EDGE('',*,*,#2209,.T.);
#3147=ORIENTED_EDGE('',*,*,#2217,.T.);
#3148=ORIENTED_EDGE('',*,*,#2214,.F.);
#3149=ORIENTED_EDGE('',*,*,#2217,.F.);
#3150=ORIENTED_EDGE('',*,*,#2208,.F.);
#3151=ORIENTED_EDGE('',*,*,#2212,.F.);
#3152=ORIENTED_EDGE('',*,*,#2215,.F.);
#3153=ORIENTED_EDGE('',*,*,#2199,.T.);
#3154=ORIENTED_EDGE('',*,*,#2203,.T.);
#3155=ORIENTED_EDGE('',*,*,#2218,.F.);
#3156=ORIENTED_EDGE('',*,*,#2219,.F.);
#3157=ORIENTED_EDGE('',*,*,#2200,.T.);
#3158=ORIENTED_EDGE('',*,*,#2219,.T.);
#3159=ORIENTED_EDGE('',*,*,#2220,.F.);
#3160=ORIENTED_EDGE('',*,*,#2204,.F.);
#3161=ORIENTED_EDGE('',*,*,#2185,.T.);
#3162=ORIENTED_EDGE('',*,*,#2195,.T.);
#3163=ORIENTED_EDGE('',*,*,#2192,.T.);
#3164=ORIENTED_EDGE('',*,*,#2189,.T.);
#3165=ORIENTED_EDGE('',*,*,#2206,.T.);
#3166=ORIENTED_EDGE('',*,*,#2216,.T.);
#3167=ORIENTED_EDGE('',*,*,#2213,.T.);
#3168=ORIENTED_EDGE('',*,*,#2210,.T.);
#3169=ORIENTED_EDGE('',*,*,#2202,.T.);
#3170=ORIENTED_EDGE('',*,*,#2205,.T.);
#3171=ORIENTED_EDGE('',*,*,#2220,.T.);
#3172=ORIENTED_EDGE('',*,*,#2218,.T.);
#3381=ADVANCED_FACE('',(#439),#250,.F.);
#3382=ADVANCED_FACE('',(#440),#251,.F.);
#3383=ADVANCED_FACE('',(#441),#252,.F.);
#3384=ADVANCED_FACE('',(#442),#253,.F.);
#3385=ADVANCED_FACE('',(#443,#123),#254,.F.);
#3386=ADVANCED_FACE('',(#444),#255,.T.);
#3387=ADVANCED_FACE('',(#445),#256,.T.);
#3388=ADVANCED_FACE('',(#446),#257,.F.);
#3389=ADVANCED_FACE('',(#447),#258,.F.);
#3390=ADVANCED_FACE('',(#448),#259,.F.);
#3391=ADVANCED_FACE('',(#449),#260,.F.);
#3392=ADVANCED_FACE('',(#450),#261,.F.);
#3393=ADVANCED_FACE('',(#451),#262,.T.);
#3394=ADVANCED_FACE('',(#452),#263,.T.);
#3395=ADVANCED_FACE('',(#453,#124),#264,.T.);
#3396=ADVANCED_FACE('',(#454),#265,.T.);
#3406=CLOSED_SHELL('',(#3381,#3382,#3383,#3384,#3385,#3386,#3387,#3388,
#3389,#3390,#3391,#3392,#3393,#3394,#3395,#3396));
#3865=AXIS2_PLACEMENT_3D('',#6937,#4844,#4845);
#3866=AXIS2_PLACEMENT_3D('',#6938,#4846,#4847);
#3867=AXIS2_PLACEMENT_3D('',#6947,#4852,#4853);
#3868=AXIS2_PLACEMENT_3D('',#6953,#4857,#4858);
#3869=AXIS2_PLACEMENT_3D('',#6959,#4862,#4863);
#3870=AXIS2_PLACEMENT_3D('',#6962,#4866,#4867);
#3871=AXIS2_PLACEMENT_3D('',#6971,#4872,#4873);
#3872=AXIS2_PLACEMENT_3D('',#6977,#4877,#4878);
#3873=AXIS2_PLACEMENT_3D('',#6981,#4881,#4882);
#3874=AXIS2_PLACEMENT_3D('',#6990,#4887,#4888);
#3875=AXIS2_PLACEMENT_3D('',#6996,#4892,#4893);
#3876=AXIS2_PLACEMENT_3D('',#7002,#4897,#4898);
#3877=AXIS2_PLACEMENT_3D('',#7005,#4901,#4902);
#3878=AXIS2_PLACEMENT_3D('',#7006,#4903,#4904);
#3879=AXIS2_PLACEMENT_3D('',#7010,#4907,#4908);
#3880=AXIS2_PLACEMENT_3D('',#7012,#4910,#4911);
#3881=AXIS2_PLACEMENT_3D('',#7013,#4912,#4913);
#4844=DIRECTION('axis',(0.,0.,1.));
#4845=DIRECTION('refdir',(1.,0.,0.));
#4846=DIRECTION('center_axis',(0.,1.,0.));
#4847=DIRECTION('ref_axis',(1.,0.,0.));
#4848=DIRECTION('',(1.,0.,0.));
#4849=DIRECTION('',(0.,0.,-1.));
#4850=DIRECTION('',(1.,0.,0.));
#4851=DIRECTION('',(0.,0.,-1.));
#4852=DIRECTION('center_axis',(1.,-1.03276560430247E-15,0.));
#4853=DIRECTION('ref_axis',(-1.03276560430247E-15,-1.,0.));
#4854=DIRECTION('',(-1.03276560430247E-15,-1.,0.));
#4855=DIRECTION('',(0.,0.,-1.));
#4856=DIRECTION('',(-1.03276560430247E-15,-1.,0.));
#4857=DIRECTION('center_axis',(0.,-1.,0.));
#4858=DIRECTION('ref_axis',(-1.,0.,0.));
#4859=DIRECTION('',(-1.,0.,0.));
#4860=DIRECTION('',(0.,0.,-1.));
#4861=DIRECTION('',(-1.,0.,0.));
#4862=DIRECTION('center_axis',(-1.,1.03276560430247E-15,0.));
#4863=DIRECTION('ref_axis',(1.03276560430247E-15,1.,0.));
#4864=DIRECTION('',(1.03276560430247E-15,1.,0.));
#4865=DIRECTION('',(1.03276560430247E-15,1.,0.));
#4866=DIRECTION('center_axis',(0.,0.,-1.));
#4867=DIRECTION('ref_axis',(-1.,0.,0.));
#4868=DIRECTION('',(1.,0.,0.));
#4869=DIRECTION('',(0.,1.,0.));
#4870=DIRECTION('',(-1.,0.,0.));
#4871=DIRECTION('',(0.,-1.,0.));
#4872=DIRECTION('center_axis',(-1.,0.,0.));
#4873=DIRECTION('ref_axis',(0.,1.,0.));
#4874=DIRECTION('',(0.,0.,-1.));
#4875=DIRECTION('',(0.,1.,0.));
#4876=DIRECTION('',(0.,0.,-1.));
#4877=DIRECTION('center_axis',(0.,1.,0.));
#4878=DIRECTION('ref_axis',(1.,0.,0.));
#4879=DIRECTION('',(0.,0.,-1.));
#4880=DIRECTION('',(1.,0.,0.));
#4881=DIRECTION('center_axis',(1.,0.,0.));
#4882=DIRECTION('ref_axis',(0.,-1.,0.));
#4883=DIRECTION('',(0.,-1.,0.));
#4884=DIRECTION('',(0.,0.,-1.));
#4885=DIRECTION('',(0.,-1.,0.));
#4886=DIRECTION('',(0.,0.,-1.));
#4887=DIRECTION('center_axis',(0.,1.,0.));
#4888=DIRECTION('ref_axis',(1.,0.,0.));
#4889=DIRECTION('',(1.,0.,0.));
#4890=DIRECTION('',(0.,0.,-1.));
#4891=DIRECTION('',(1.,0.,0.));
#4892=DIRECTION('center_axis',(-1.,0.,0.));
#4893=DIRECTION('ref_axis',(0.,1.,0.));
#4894=DIRECTION('',(0.,1.,0.));
#4895=DIRECTION('',(0.,0.,-1.));
#4896=DIRECTION('',(0.,1.,0.));
#4897=DIRECTION('center_axis',(0.,-1.,0.));
#4898=DIRECTION('ref_axis',(-1.,0.,0.));
#4899=DIRECTION('',(-1.,0.,0.));
#4900=DIRECTION('',(-1.,0.,0.));
#4901=DIRECTION('center_axis',(0.,0.,-1.));
#4902=DIRECTION('ref_axis',(-1.,0.,0.));
#4903=DIRECTION('center_axis',(0.,-1.,0.));
#4904=DIRECTION('ref_axis',(-1.,0.,0.));
#4905=DIRECTION('',(-1.,0.,0.));
#4906=DIRECTION('',(0.,0.,-1.));
#4907=DIRECTION('center_axis',(1.,0.,0.));
#4908=DIRECTION('ref_axis',(0.,-1.,0.));
#4909=DIRECTION('',(0.,-1.,0.));
#4910=DIRECTION('center_axis',(0.,0.,1.));
#4911=DIRECTION('ref_axis',(-1.,0.,0.));
#4912=DIRECTION('center_axis',(0.,0.,-1.));
#4913=DIRECTION('ref_axis',(-1.,0.,0.));
#6937=CARTESIAN_POINT('',(0.,0.,0.));
#6938=CARTESIAN_POINT('Origin',(-24.3,-11.4095206243716,16.));
#6939=CARTESIAN_POINT('',(-24.3,-11.4095206243716,16.));
#6940=CARTESIAN_POINT('',(24.3,-11.4095206243716,16.));
#6941=CARTESIAN_POINT('',(-12.15,-11.4095206243716,16.));
#6942=CARTESIAN_POINT('',(-24.3,-11.4095206243716,15.9));
#6943=CARTESIAN_POINT('',(-24.3,-11.4095206243716,16.));
#6944=CARTESIAN_POINT('',(24.3,-11.4095206243716,15.9));
#6945=CARTESIAN_POINT('',(-24.3,-11.4095206243716,15.9));
#6946=CARTESIAN_POINT('',(24.3,-11.4095206243716,16.));
#6947=CARTESIAN_POINT('Origin',(-24.3,-2.80952062437159,16.));
#6948=CARTESIAN_POINT('',(-24.3,-2.80952062437159,16.));
#6949=CARTESIAN_POINT('',(-24.3,-4.95952062437158,16.));
#6950=CARTESIAN_POINT('',(-24.3,-2.80952062437159,15.9));
#6951=CARTESIAN_POINT('',(-24.3,-2.80952062437159,16.));
#6952=CARTESIAN_POINT('',(-24.3,-2.80952062437159,15.9));
#6953=CARTESIAN_POINT('Origin',(24.3,-2.80952062437159,16.));
#6954=CARTESIAN_POINT('',(24.3,-2.80952062437159,16.));
#6955=CARTESIAN_POINT('',(12.15,-2.80952062437159,16.));
#6956=CARTESIAN_POINT('',(24.3,-2.80952062437159,15.9));
#6957=CARTESIAN_POINT('',(24.3,-2.80952062437159,16.));
#6958=CARTESIAN_POINT('',(24.3,-2.80952062437159,15.9));
#6959=CARTESIAN_POINT('Origin',(24.3,-11.4095206243716,16.));
#6960=CARTESIAN_POINT('',(24.3,-9.2595206243716,16.));
#6961=CARTESIAN_POINT('',(24.3,-11.4095206243716,15.9));
#6962=CARTESIAN_POINT('Origin',(0.,-7.10952062437159,15.9));
#6963=CARTESIAN_POINT('',(-25.,-2.10952062437159,15.9));
#6964=CARTESIAN_POINT('',(25.,-2.10952062437159,15.9));
#6965=CARTESIAN_POINT('',(-12.5,-2.10952062437159,15.9));
#6966=CARTESIAN_POINT('',(-25.,-12.1095206243716,15.9));
#6967=CARTESIAN_POINT('',(-25.,-9.60952062437159,15.9));
#6968=CARTESIAN_POINT('',(25.,-12.1095206243716,15.9));
#6969=CARTESIAN_POINT('',(12.5,-12.1095206243716,15.9));
#6970=CARTESIAN_POINT('',(25.,-4.60952062437159,15.9));
#6971=CARTESIAN_POINT('Origin',(-25.,-12.1095206243716,16.));
#6972=CARTESIAN_POINT('',(-25.,-2.10952062437159,15.));
#6973=CARTESIAN_POINT('',(-25.,-2.10952062437159,16.));
#6974=CARTESIAN_POINT('',(-25.,-12.1095206243716,15.));
#6975=CARTESIAN_POINT('',(-25.,-2.10952062437159,15.));
#6976=CARTESIAN_POINT('',(-25.,-12.1095206243716,16.));
#6977=CARTESIAN_POINT('Origin',(-25.,-2.10952062437159,16.));
#6978=CARTESIAN_POINT('',(25.,-2.10952062437159,15.));
#6979=CARTESIAN_POINT('',(25.,-2.10952062437159,16.));
#6980=CARTESIAN_POINT('',(25.,-2.10952062437159,15.));
#6981=CARTESIAN_POINT('Origin',(22.,-5.60952062437159,16.));
#6982=CARTESIAN_POINT('',(22.,-5.60952062437159,16.));
#6983=CARTESIAN_POINT('',(22.,-8.60952062437159,16.));
#6984=CARTESIAN_POINT('',(22.,-6.35952062437159,16.));
#6985=CARTESIAN_POINT('',(22.,-5.60952062437159,15.9));
#6986=CARTESIAN_POINT('',(22.,-5.60952062437159,16.));
#6987=CARTESIAN_POINT('',(22.,-8.60952062437159,15.9));
#6988=CARTESIAN_POINT('',(22.,-5.60952062437159,15.9));
#6989=CARTESIAN_POINT('',(22.,-8.60952062437159,16.));
#6990=CARTESIAN_POINT('Origin',(-22.,-5.60952062437159,16.));
#6991=CARTESIAN_POINT('',(-22.,-5.60952062437159,16.));
#6992=CARTESIAN_POINT('',(-11.,-5.60952062437159,16.));
#6993=CARTESIAN_POINT('',(-22.,-5.60952062437159,15.9));
#6994=CARTESIAN_POINT('',(-22.,-5.60952062437159,16.));
#6995=CARTESIAN_POINT('',(-22.,-5.60952062437159,15.9));
#6996=CARTESIAN_POINT('Origin',(-22.,-8.60952062437159,16.));
#6997=CARTESIAN_POINT('',(-22.,-8.60952062437159,16.));
#6998=CARTESIAN_POINT('',(-22.,-7.85952062437159,16.));
#6999=CARTESIAN_POINT('',(-22.,-8.60952062437159,15.9));
#7000=CARTESIAN_POINT('',(-22.,-8.60952062437159,16.));
#7001=CARTESIAN_POINT('',(-22.,-8.60952062437159,15.9));
#7002=CARTESIAN_POINT('Origin',(22.,-8.60952062437159,16.));
#7003=CARTESIAN_POINT('',(11.,-8.60952062437159,16.));
#7004=CARTESIAN_POINT('',(22.,-8.60952062437159,15.9));
#7005=CARTESIAN_POINT('Origin',(0.,-7.10952062437159,15.9));
#7006=CARTESIAN_POINT('Origin',(25.,-12.1095206243716,16.));
#7007=CARTESIAN_POINT('',(25.,-12.1095206243716,15.));
#7008=CARTESIAN_POINT('',(-25.,-12.1095206243716,15.));
#7009=CARTESIAN_POINT('',(25.,-12.1095206243716,16.));
#7010=CARTESIAN_POINT('Origin',(25.,-2.10952062437159,16.));
#7011=CARTESIAN_POINT('',(25.,-12.1095206243716,15.));
#7012=CARTESIAN_POINT('Origin',(0.,-7.10952062437159,16.));
#7013=CARTESIAN_POINT('Origin',(0.,-7.10952062437159,15.));
#7034=UNCERTAINTY_MEASURE_WITH_UNIT(LENGTH_MEASURE(0.01),#7048,
'DISTANCE_ACCURACY_VALUE',
'Maximum model space distance between geometric entities at asserted c
onnectivities');
#7035=UNCERTAINTY_MEASURE_WITH_UNIT(LENGTH_MEASURE(0.01),#7048,
'DISTANCE_ACCURACY_VALUE',
'Maximum model space distance between geometric entities at asserted c
onnectivities');
#7046=(
GEOMETRIC_REPRESENTATION_CONTEXT(3)
GLOBAL_UNCERTAINTY_ASSIGNED_CONTEXT((#7034))
GLOBAL_UNIT_ASSIGNED_CONTEXT((#7048,#7050,#7051))
REPRESENTATION_CONTEXT('','3D')
);
#7047=(
GEOMETRIC_REPRESENTATION_CONTEXT(3)
GLOBAL_UNCERTAINTY_ASSIGNED_CONTEXT((#7035))
GLOBAL_UNIT_ASSIGNED_CONTEXT((#7048,#7050,#7051))
REPRESENTATION_CONTEXT('','3D')
);
#7048=(
LENGTH_UNIT()
NAMED_UNIT(*)
SI_UNIT(.MILLI.,.METRE.)
);
#7050=(
NAMED_UNIT(*)
PLANE_ANGLE_UNIT()
SI_UNIT($,.RADIAN.)
);
#7051=(
NAMED_UNIT(*)
SI_UNIT($,.STERADIAN.)
SOLID_ANGLE_UNIT()
);
#7062=SHAPE_DEFINITION_REPRESENTATION(#7073,#7094);
#7073=PRODUCT_DEFINITION_SHAPE('',$,#7106);
#7094=SHAPE_REPRESENTATION('',(#3865),#7046);
#7095=PRODUCT_DEFINITION_CONTEXT('part definition',#7130,'design');
#7106=PRODUCT_DEFINITION('Circuit','Circuit',#7117,#7095);
#7117=PRODUCT_DEFINITION_FORMATION('',$,#7142);
#7130=APPLICATION_CONTEXT(
'Core Data for Automotive Mechanical Design Process');
#7131=PRODUCT_CONTEXT('part definition',#7130,'mechanical');
#7142=PRODUCT('Circuit','Circuit',$,(#7131));
#7206=COLOUR_RGB('Off White',0.89,0.88,0.83);
#7207=FILL_AREA_STYLE_COLOUR('',#7206);
#7208=FILL_AREA_STYLE('',(#7207));
#7209=SURFACE_STYLE_FILL_AREA(#7208);
#7210=SURFACE_SIDE_STYLE('',(#7209));
#7211=SURFACE_STYLE_USAGE(.BOTH.,#7210);
#7212=PRESENTATION_STYLE_ASSIGNMENT((#7211));
ENDSEC;
END-ISO-10303-21;
